ISO-10303-21;
HEADER;
FILE_DESCRIPTION (('STEP AP214'),
    '1' );
FILE_NAME ('roller axis assy_r4.step',
    '2026-10-24T11:01:53',
    ( '' ),
    ( '' ),
    'SwSTEP 2.0',
    'SolidWorks 2026',
    '' );
FILE_SCHEMA (( 'AUTOMOTIVE_DESIGN' ));
ENDSEC;

DATA;
#11=EDGE_CURVE ( 'NONE', #6628, #4697, #895, .T. ) ;
#19=FACE_BOUND ( 'NONE', #2899, .T. ) ;
#23=AXIS2_PLACEMENT_3D ( 'NONE', #2020, #5963, #7409 ) ;
#35=VERTEX_POINT ( 'NONE', #5063 ) ;
#52=EDGE_LOOP ( 'NONE', ( #3037, #7373 ) ) ;
#61=ORIENTED_EDGE ( 'NONE', *, *, #1740, .F. ) ;
#65=( NAMED_UNIT ( * ) PLANE_ANGLE_UNIT ( ) SI_UNIT ( $, .RADIAN. ) );
#75=CIRCLE ( 'NONE', #7173, 10.00000000000000000 ) ;
#86=DIRECTION ( 'NONE',  ( -0.000000000000000000, -0.000000000000000000, -1.000000000000000000 ) ) ;
#104=VERTEX_POINT ( 'NONE', #727 ) ;
#112=CARTESIAN_POINT ( 'NONE',  ( 5.000000000000000000, -5.000000000000000000, -36.00000000000000000 ) ) ;
#114=CARTESIAN_POINT ( 'NONE',  ( 0.000000000000000000, 0.000000000000000000, 120.0000000000000284 ) ) ;
#120=EDGE_CURVE ( 'NONE', #6932, #5212, #7298, .T. ) ;
#140=LINE ( 'NONE', #6246, #2728 ) ;
#145=( NAMED_UNIT ( * ) SI_UNIT ( $, .STERADIAN. ) SOLID_ANGLE_UNIT ( ) );
#157=CARTESIAN_POINT ( 'NONE',  ( -5.000000000000001776, 5.000000000000001776, -36.00000000000000000 ) ) ;
#159=EDGE_LOOP ( 'NONE', ( #3695, #3628, #3551, #216 ) ) ;
#166=CARTESIAN_POINT ( 'NONE',  ( 20.00000000000000000, 0.000000000000000000, -7.999999999999992895 ) ) ;
#204=DIRECTION ( 'NONE',  ( 0.000000000000000000, -0.000000000000000000, 1.000000000000000000 ) ) ;
#209=AXIS2_PLACEMENT_3D ( 'NONE', #6688, #3397, #6036 ) ;
#216=ORIENTED_EDGE ( 'NONE', *, *, #6684, .T. ) ;
#221=CARTESIAN_POINT ( 'NONE',  ( 5.000000000000000000, 5.000000000000000000, 140.0000000000000000 ) ) ;
#222=DIRECTION ( 'NONE',  ( -0.000000000000000000, -0.000000000000000000, -1.000000000000000000 ) ) ;
#230=DIRECTION ( 'NONE',  ( -0.000000000000000000, -0.000000000000000000, 1.000000000000000000 ) ) ;
#232=DIRECTION ( 'NONE',  ( 0.000000000000000000, -0.000000000000000000, 1.000000000000000000 ) ) ;
#247=PLANE ( 'NONE',  #2215 ) ;
#269=DIRECTION ( 'NONE',  ( -1.000000000000000000, 0.000000000000000000, 0.000000000000000000 ) ) ;
#277=ORIENTED_EDGE ( 'NONE', *, *, #6684, .F. ) ;
#278=DIRECTION ( 'NONE',  ( 0.000000000000000000, 0.000000000000000000, -1.000000000000000000 ) ) ;
#281=DIRECTION ( 'NONE',  ( 0.000000000000000000, 0.000000000000000000, 1.000000000000000000 ) ) ;
#282=EDGE_CURVE ( 'NONE', #4949, #5455, #6249, .T. ) ;
#286=EDGE_LOOP ( 'NONE', ( #7427, #1240, #4470, #6347 ) ) ;
#294=DIRECTION ( 'NONE',  ( 1.000000000000000000, 1.734723475976806848E-16, 0.000000000000000000 ) ) ;
#299=EDGE_CURVE ( 'NONE', #6060, #4780, #4987, .T. ) ;
#306=EDGE_CURVE ( 'NONE', #5455, #35, #2943, .T. ) ;
#317=CIRCLE ( 'NONE', #5184, 20.00000000000000000 ) ;
#342=VERTEX_POINT ( 'NONE', #5637 ) ;
#357=DIRECTION ( 'NONE',  ( 1.734723475976806848E-16, -1.000000000000000000, -0.000000000000000000 ) ) ;
#362=VECTOR ( 'NONE', #6205, 1000.000000000000000 ) ;
#380=CARTESIAN_POINT ( 'NONE',  ( 0.000000000000000000, 0.000000000000000000, -7.999999999999996447 ) ) ;
#390=AXIS2_PLACEMENT_3D ( 'NONE', #5308, #6267, #5487 ) ;
#391=DIRECTION ( 'NONE',  ( 1.000000000000000000, 0.000000000000000000, 0.000000000000000000 ) ) ;
#419=EDGE_LOOP ( 'NONE', ( #6359, #5460, #4136, #4345 ) ) ;
#428=VERTEX_POINT ( 'NONE', #5200 ) ;
#443=CARTESIAN_POINT ( 'NONE',  ( -5.000000000000001776, 5.000000000000001776, -36.00000000000000000 ) ) ;
#464=DIRECTION ( 'NONE',  ( 0.000000000000000000, 0.000000000000000000, 1.000000000000000000 ) ) ;
#490=CARTESIAN_POINT ( 'NONE',  ( -5.000000000000001776, 5.000000000000001776, 148.0000000000000284 ) ) ;
#498=FACE_BOUND ( 'NONE', #7702, .T. ) ;
#506=EDGE_LOOP ( 'NONE', ( #6682, #4119, #1543, #7518 ) ) ;
#521=ORIENTED_EDGE ( 'NONE', *, *, #2052, .T. ) ;
#531=DIRECTION ( 'NONE',  ( -1.000000000000000000, 1.734723475976806848E-16, -0.000000000000000000 ) ) ;
#548=ADVANCED_FACE ( 'NONE', ( #2464 ), #6493, .F. ) ;
#560=CARTESIAN_POINT ( 'NONE',  ( 5.000000000000000000, -5.000000000000000000, 148.0000000000000284 ) ) ;
#563=VERTEX_POINT ( 'NONE', #6362 ) ;
#564=( NAMED_UNIT ( * ) PLANE_ANGLE_UNIT ( ) SI_UNIT ( $, .RADIAN. ) );
#572=CARTESIAN_POINT ( 'NONE',  ( 0.000000000000000000, 0.000000000000000000, -27.99999999999999645 ) ) ;
#594=AXIS2_PLACEMENT_3D ( 'NONE', #3123, #464, #5764 ) ;
#613=SURFACE_STYLE_USAGE ( .BOTH. , #5951 ) ;
#619=ORIENTED_EDGE ( 'NONE', *, *, #306, .T. ) ;
#621=CARTESIAN_POINT ( 'NONE',  ( -10.00000000000000000, 1.224646799147353059E-15, -27.99999999999999645 ) ) ;
#624=FACE_OUTER_BOUND ( 'NONE', #6447, .T. ) ;
#638=SHAPE_REPRESENTATION ( 'roller axis assy_r4', ( #594 ), #1694 ) ;
#657=( LENGTH_UNIT ( ) NAMED_UNIT ( * ) SI_UNIT ( .MILLI., .METRE. ) );
#695=DIRECTION ( 'NONE',  ( 0.000000000000000000, 0.000000000000000000, 1.000000000000000000 ) ) ;
#697=( NAMED_UNIT ( * ) SI_UNIT ( $, .STERADIAN. ) SOLID_ANGLE_UNIT ( ) );
#721=( GEOMETRIC_REPRESENTATION_CONTEXT ( 3 ) GLOBAL_UNCERTAINTY_ASSIGNED_CONTEXT ( ( #3933 ) ) GLOBAL_UNIT_ASSIGNED_CONTEXT ( ( #6030, #65, #145 ) ) REPRESENTATION_CONTEXT ( 'NONE', 'WORKASPACE' ) );
#727=CARTESIAN_POINT ( 'NONE',  ( 5.000000000000000000, -5.000000000000000000, 140.0000000000000000 ) ) ;
#743=( LENGTH_UNIT ( ) NAMED_UNIT ( * ) SI_UNIT ( .MILLI., .METRE. ) );
#761=VECTOR ( 'NONE', #8600, 1000.000000000000000 ) ;
#772=CARTESIAN_POINT ( 'NONE',  ( 0.000000000000000000, 0.000000000000000000, 140.0000000000000000 ) ) ;
#775=CARTESIAN_POINT ( 'NONE',  ( 5.000000000000000000, -5.000000000000000000, 148.0000000000000284 ) ) ;
#787=VECTOR ( 'NONE', #230, 1000.000000000000000 ) ;
#793=AXIS2_PLACEMENT_3D ( 'NONE', #3331, #7235, #6502 ) ;
#795=VECTOR ( 'NONE', #4140, 1000.000000000000000 ) ;
#800=FACE_OUTER_BOUND ( 'NONE', #286, .T. ) ;
#810=CARTESIAN_POINT ( 'NONE',  ( -5.000000000000000000, -5.000000000000000000, 148.0000000000000284 ) ) ;
#830=EDGE_CURVE ( 'NONE', #5455, #1089, #967, .T. ) ;
#838=ORIENTED_EDGE ( 'NONE', *, *, #2052, .F. ) ;
#854=DIRECTION ( 'NONE',  ( 1.000000000000000000, 0.000000000000000000, 0.000000000000000000 ) ) ;
#862=ORIENTED_EDGE ( 'NONE', *, *, #1306, .F. ) ;
#882=DIRECTION ( 'NONE',  ( 0.000000000000000000, 0.000000000000000000, 1.000000000000000000 ) ) ;
#884=VERTEX_POINT ( 'NONE', #166 ) ;
#895=LINE ( 'NONE', #6196, #787 ) ;
#899=EDGE_CURVE ( 'NONE', #884, #8142, #2838, .T. ) ;
#935=VECTOR ( 'NONE', #357, 1000.000000000000000 ) ;
#967=LINE ( 'NONE', #3617, #795 ) ;
#990=CARTESIAN_POINT ( 'NONE',  ( -20.00000000000000000, 2.449293598294706513E-15, -84.56854249492380404 ) ) ;
#994=CARTESIAN_POINT ( 'NONE',  ( -5.000000000000000000, -5.000000000000000000, 140.0000000000000000 ) ) ;
#1001=ORIENTED_EDGE ( 'NONE', *, *, #282, .F. ) ;
#1003=LINE ( 'NONE', #3657, #761 ) ;
#1015=DIRECTION ( 'NONE',  ( 1.000000000000000000, 0.000000000000000000, -0.000000000000000000 ) ) ;
#1047=ORIENTED_EDGE ( 'NONE', *, *, #1141, .T. ) ;
#1070=AXIS2_PLACEMENT_3D ( 'NONE', #7504, #6235, #269 ) ;
#1085=ORIENTED_EDGE ( 'NONE', *, *, #1626, .F. ) ;
#1087=DIRECTION ( 'NONE',  ( 0.000000000000000000, 0.000000000000000000, -1.000000000000000000 ) ) ;
#1088=ORIENTED_EDGE ( 'NONE', *, *, #2206, .F. ) ;
#1089=VERTEX_POINT ( 'NONE', #8017 ) ;
#1139=ORIENTED_EDGE ( 'NONE', *, *, #4828, .F. ) ;
#1141=EDGE_CURVE ( 'NONE', #6628, #563, #8296, .T. ) ;
#1177=ORIENTED_EDGE ( 'NONE', *, *, #4810, .T. ) ;
#1218=CARTESIAN_POINT ( 'NONE',  ( -5.000000000000001776, 5.000000000000001776, 140.0000000000000000 ) ) ;
#1221=DIRECTION ( 'NONE',  ( 1.000000000000000000, 0.000000000000000000, 0.000000000000000000 ) ) ;
#1234=CIRCLE ( 'NONE', #3737, 10.00000000000000000 ) ;
#1240=ORIENTED_EDGE ( 'NONE', *, *, #4828, .T. ) ;
#1260=DIRECTION ( 'NONE',  ( -1.000000000000000000, 0.000000000000000000, -0.000000000000000000 ) ) ;
#1268=DIRECTION ( 'NONE',  ( -0.000000000000000000, -0.000000000000000000, 1.000000000000000000 ) ) ;
#1271=LINE ( 'NONE', #621, #8385 ) ;
#1274=PLANE ( 'NONE',  #7841 ) ;
#1306=EDGE_CURVE ( 'NONE', #4697, #6157, #1633, .T. ) ;
#1345=PRODUCT_DEFINITION_SHAPE ( 'NONE', 'NONE',  #7229 ) ;
#1358=LINE ( 'NONE', #7366, #1980 ) ;
#1384=CARTESIAN_POINT ( 'NONE',  ( -5.000000000000001776, 5.000000000000001776, -27.99999999999999645 ) ) ;
#1394=EDGE_LOOP ( 'NONE', ( #4253, #277, #2109, #1643 ) ) ;
#1447=CARTESIAN_POINT ( 'NONE',  ( 5.000000000000000000, -5.000000000000000000, -27.99999999999999645 ) ) ;
#1457=ORIENTED_EDGE ( 'NONE', *, *, #2206, .T. ) ;
#1477=AXIS2_PLACEMENT_3D ( 'NONE', #3255, #4683, #5896 ) ;
#1496=DIRECTION ( 'NONE',  ( 1.000000000000000000, 1.734723475976806848E-16, -0.000000000000000000 ) ) ;
#1539=EDGE_CURVE ( 'NONE', #6157, #4697, #2592, .T. ) ;
#1543=ORIENTED_EDGE ( 'NONE', *, *, #6736, .F. ) ;
#1580=EDGE_LOOP ( 'NONE', ( #2944, #1732, #5125, #1177 ) ) ;
#1589=EDGE_CURVE ( 'NONE', #8480, #6268, #75, .T. ) ;
#1626=EDGE_CURVE ( 'NONE', #428, #4949, #140, .T. ) ;
#1627=CIRCLE ( 'NONE', #1070, 20.00000000000000000 ) ;
#1629=FACE_BOUND ( 'NONE', #2134, .T. ) ;
#1632=CARTESIAN_POINT ( 'NONE',  ( -5.000000000000001776, 5.000000000000001776, -27.99999999999999645 ) ) ;
#1633=CIRCLE ( 'NONE', #1897, 10.00000000000000000 ) ;
#1643=ORIENTED_EDGE ( 'NONE', *, *, #3986, .T. ) ;
#1686=DIRECTION ( 'NONE',  ( 0.000000000000000000, -1.000000000000000000, 0.000000000000000000 ) ) ;
#1694=( GEOMETRIC_REPRESENTATION_CONTEXT ( 3 ) GLOBAL_UNCERTAINTY_ASSIGNED_CONTEXT ( ( #6372 ) ) GLOBAL_UNIT_ASSIGNED_CONTEXT ( ( #657, #2057, #697 ) ) REPRESENTATION_CONTEXT ( 'NONE', 'WORKASPACE' ) );
#1719=AXIS2_PLACEMENT_3D ( 'NONE', #2690, #7168, #7912 ) ;
#1732=ORIENTED_EDGE ( 'NONE', *, *, #3986, .F. ) ;
#1740=EDGE_CURVE ( 'NONE', #1089, #3680, #4421, .T. ) ;
#1774=VECTOR ( 'NONE', #882, 1000.000000000000000 ) ;
#1794=ORIENTED_EDGE ( 'NONE', *, *, #2131, .F. ) ;
#1816=VECTOR ( 'NONE', #222, 1000.000000000000000 ) ;
#1830=DIRECTION ( 'NONE',  ( -1.734723475976806848E-16, 1.000000000000000000, 0.000000000000000000 ) ) ;
#1849=DIRECTION ( 'NONE',  ( -1.734723475976806848E-16, -1.000000000000000000, 0.000000000000000000 ) ) ;
#1856=FACE_OUTER_BOUND ( 'NONE', #7743, .T. ) ;
#1872=ADVANCED_FACE ( 'NONE', ( #3858 ), #3286, .F. ) ;
#1889=EDGE_CURVE ( 'NONE', #3427, #4515, #5927, .T. ) ;
#1897=AXIS2_PLACEMENT_3D ( 'NONE', #380, #4995, #2998 ) ;
#1900=ADVANCED_BREP_SHAPE_REPRESENTATION ( '', ( #4686, #594 ), #1694 ) ;
#1952=EDGE_CURVE ( 'NONE', #4515, #7275, #5197, .T. ) ;
#1980=VECTOR ( 'NONE', #86, 1000.000000000000000 ) ;
#2020=CARTESIAN_POINT ( 'NONE',  ( 0.000000000000000000, 0.000000000000000000, -27.99999999999999645 ) ) ;
#2026=DIRECTION ( 'NONE',  ( 0.000000000000000000, 0.000000000000000000, -1.000000000000000000 ) ) ;
#2052=EDGE_CURVE ( 'NONE', #6060, #884, #1627, .T. ) ;
#2057=( NAMED_UNIT ( * ) PLANE_ANGLE_UNIT ( ) SI_UNIT ( $, .RADIAN. ) );
#2066=PLANE ( 'NONE',  #4065 ) ;
#2078=ORIENTED_EDGE ( 'NONE', *, *, #3296, .T. ) ;
#2086=LINE ( 'NONE', #4166, #8523 ) ;
#2095=PLANE ( 'NONE',  #8120 ) ;
#2109=ORIENTED_EDGE ( 'NONE', *, *, #5103, .F. ) ;
#2131=EDGE_CURVE ( 'NONE', #7651, #7275, #7730, .T. ) ;
#2134=EDGE_LOOP ( 'NONE', ( #6237, #1088 ) ) ;
#2181=VERTEX_POINT ( 'NONE', #1632 ) ;
#2206=EDGE_CURVE ( 'NONE', #8570, #342, #3160, .T. ) ;
#2215=AXIS2_PLACEMENT_3D ( 'NONE', #112, #6170, #204 ) ;
#2216=ADVANCED_FACE ( 'NONE', ( #4618 ), #2509, .T. ) ;
#2241=EDGE_LOOP ( 'NONE', ( #6031, #2559, #1085, #3839 ) ) ;
#2250=DIRECTION ( 'NONE',  ( 1.000000000000000000, 0.000000000000000000, 0.000000000000000000 ) ) ;
#2262=ADVANCED_FACE ( 'NONE', ( #3321 ), #8505, .F. ) ;
#2265=EDGE_CURVE ( 'NONE', #4949, #2181, #6120, .T. ) ;
#2277=VECTOR ( 'NONE', #5213, 1000.000000000000000 ) ;
#2300=CARTESIAN_POINT ( 'NONE',  ( -5.000000000000001776, 5.000000000000001776, 140.0000000000000000 ) ) ;
#2308=ORIENTED_EDGE ( 'NONE', *, *, #5103, .T. ) ;
#2333=AXIS2_PLACEMENT_3D ( 'NONE', #443, #1849, #4449 ) ;
#2414=DIRECTION ( 'NONE',  ( 0.000000000000000000, 0.000000000000000000, 1.000000000000000000 ) ) ;
#2429=AXIS2_PLACEMENT_3D ( 'NONE', #810, #6720, #232 ) ;
#2464=FACE_OUTER_BOUND ( 'NONE', #4631, .T. ) ;
#2468=EDGE_CURVE ( 'NONE', #884, #6060, #7909, .T. ) ;
#2509=CYLINDRICAL_SURFACE ( 'NONE', #7752, 10.00000000000000000 ) ;
#2536=( GEOMETRIC_REPRESENTATION_CONTEXT ( 3 ) GLOBAL_UNCERTAINTY_ASSIGNED_CONTEXT ( ( #7071 ) ) GLOBAL_UNIT_ASSIGNED_CONTEXT ( ( #743, #564, #4743 ) ) REPRESENTATION_CONTEXT ( 'NONE', 'WORKASPACE' ) );
#2537=DIRECTION ( 'NONE',  ( 0.000000000000000000, 0.000000000000000000, -1.000000000000000000 ) ) ;
#2557=DIRECTION ( 'NONE',  ( -0.000000000000000000, -0.000000000000000000, -1.000000000000000000 ) ) ;
#2559=ORIENTED_EDGE ( 'NONE', *, *, #2265, .F. ) ;
#2592=CIRCLE ( 'NONE', #1477, 10.00000000000000000 ) ;
#2618=ORIENTED_EDGE ( 'NONE', *, *, #282, .T. ) ;
#2673=FACE_OUTER_BOUND ( 'NONE', #1394, .T. ) ;
#2684=ADVANCED_FACE ( 'NONE', ( #6355 ), #7761, .T. ) ;
#2690=CARTESIAN_POINT ( 'NONE',  ( 0.000000000000000000, 0.000000000000000000, 120.0000000000000142 ) ) ;
#2717=DIRECTION ( 'NONE',  ( -0.000000000000000000, -0.000000000000000000, 1.000000000000000000 ) ) ;
#2720=ADVANCED_FACE ( 'NONE', ( #6963 ), #3183, .T. ) ;
#2728=VECTOR ( 'NONE', #6768, 1000.000000000000000 ) ;
#2730=ORIENTED_EDGE ( 'NONE', *, *, #6736, .T. ) ;
#2741=EDGE_CURVE ( 'NONE', #342, #8570, #7815, .T. ) ;
#2762=CARTESIAN_POINT ( 'NONE',  ( 0.000000000000000000, 0.000000000000000000, 140.0000000000000000 ) ) ;
#2785=CYLINDRICAL_SURFACE ( 'NONE', #6793, 10.00000000000000000 ) ;
#2791=EDGE_CURVE ( 'NONE', #104, #7983, #4561, .T. ) ;
#2798=CARTESIAN_POINT ( 'NONE',  ( -5.000000000000000000, -5.000000000000000000, 148.0000000000000284 ) ) ;
#2807=DIRECTION ( 'NONE',  ( 0.000000000000000000, 0.000000000000000000, 1.000000000000000000 ) ) ;
#2838=LINE ( 'NONE', #8198, #1774 ) ;
#2899=EDGE_LOOP ( 'NONE', ( #6308, #8395, #1794, #5554 ) ) ;
#2918=DIRECTION ( 'NONE',  ( -0.000000000000000000, -0.000000000000000000, -1.000000000000000000 ) ) ;
#2921=ADVANCED_FACE ( 'NONE', ( #4133 ), #247, .F. ) ;
#2924=ADVANCED_FACE ( 'NONE', ( #4830 ), #2785, .T. ) ;
#2943=LINE ( 'NONE', #8351, #362 ) ;
#2944=ORIENTED_EDGE ( 'NONE', *, *, #2791, .T. ) ;
#2998=DIRECTION ( 'NONE',  ( -1.000000000000000000, 0.000000000000000000, 0.000000000000000000 ) ) ;
#3037=ORIENTED_EDGE ( 'NONE', *, *, #7557, .T. ) ;
#3123=CARTESIAN_POINT ( 'NONE',  ( 0.000000000000000000, 0.000000000000000000, 0.000000000000000000 ) ) ;
#3154=CARTESIAN_POINT ( 'NONE',  ( 5.000000000000000000, 5.000000000000000000, -36.00000000000000000 ) ) ;
#3160=CIRCLE ( 'NONE', #8451, 10.00000000000000000 ) ;
#3164=ORIENTED_EDGE ( 'NONE', *, *, #1306, .T. ) ;
#3183=PLANE ( 'NONE',  #3595 ) ;
#3197=DIRECTION ( 'NONE',  ( 1.000000000000000000, 0.000000000000000000, 0.000000000000000000 ) ) ;
#3221=DIRECTION ( 'NONE',  ( -1.000000000000000000, 0.000000000000000000, 0.000000000000000000 ) ) ;
#3251=CARTESIAN_POINT ( 'NONE',  ( -20.00000000000000000, 2.449293598294706513E-15, -7.999999999999992895 ) ) ;
#3255=CARTESIAN_POINT ( 'NONE',  ( 0.000000000000000000, 0.000000000000000000, -7.999999999999996447 ) ) ;
#3259=PRODUCT_CONTEXT ( 'NONE', #6576, 'mechanical' ) ;
#3267=ORIENTED_EDGE ( 'NONE', *, *, #830, .F. ) ;
#3286=PLANE ( 'NONE',  #793 ) ;
#3289=ORIENTED_EDGE ( 'NONE', *, *, #8388, .F. ) ;
#3296=EDGE_CURVE ( 'NONE', #6268, #8480, #1234, .T. ) ;
#3321=FACE_OUTER_BOUND ( 'NONE', #419, .T. ) ;
#3327=CARTESIAN_POINT ( 'NONE',  ( -5.000000000000000000, -5.000000000000000000, -27.99999999999999645 ) ) ;
#3328=CARTESIAN_POINT ( 'NONE',  ( 0.000000000000000000, 0.000000000000000000, -7.999999999999996447 ) ) ;
#3331=CARTESIAN_POINT ( 'NONE',  ( 5.000000000000000000, -5.000000000000000000, 148.0000000000000284 ) ) ;
#3340=CIRCLE ( 'NONE', #4450, 10.00000000000000000 ) ;
#3343=DIRECTION ( 'NONE',  ( 0.000000000000000000, 1.000000000000000000, 0.000000000000000000 ) ) ;
#3384=VECTOR ( 'NONE', #2250, 1000.000000000000000 ) ;
#3397=DIRECTION ( 'NONE',  ( 0.000000000000000000, 0.000000000000000000, -1.000000000000000000 ) ) ;
#3412=FACE_BOUND ( 'NONE', #4195, .T. ) ;
#3427=VERTEX_POINT ( 'NONE', #3758 ) ;
#3431=DIRECTION ( 'NONE',  ( 1.000000000000000000, -1.734723475976806848E-16, 0.000000000000000000 ) ) ;
#3432=ORIENTED_EDGE ( 'NONE', *, *, #7557, .F. ) ;
#3551=ORIENTED_EDGE ( 'NONE', *, *, #1889, .F. ) ;
#3562=ADVANCED_FACE ( 'NONE', ( #3889 ), #3716, .T. ) ;
#3595=AXIS2_PLACEMENT_3D ( 'NONE', #8496, #2537, #6313 ) ;
#3617=CARTESIAN_POINT ( 'NONE',  ( 5.000000000000000000, 5.000000000000000000, -36.00000000000000000 ) ) ;
#3621=CARTESIAN_POINT ( 'NONE',  ( -10.00000000000000000, 1.224646799147353059E-15, -27.99999999999999645 ) ) ;
#3628=ORIENTED_EDGE ( 'NONE', *, *, #1952, .F. ) ;
#3657=CARTESIAN_POINT ( 'NONE',  ( 5.000000000000000000, -5.000000000000000000, -36.00000000000000000 ) ) ;
#3680=VERTEX_POINT ( 'NONE', #1447 ) ;
#3695=ORIENTED_EDGE ( 'NONE', *, *, #2131, .T. ) ;
#3698=DIRECTION ( 'NONE',  ( -1.000000000000000000, 0.000000000000000000, 0.000000000000000000 ) ) ;
#3704=VECTOR ( 'NONE', #1686, 1000.000000000000000 ) ;
#3716=CYLINDRICAL_SURFACE ( 'NONE', #5134, 20.00000000000000000 ) ;
#3724=EDGE_LOOP ( 'NONE', ( #7143, #8545, #7925, #6967 ) ) ;
#3737=AXIS2_PLACEMENT_3D ( 'NONE', #2762, #5407, #8081 ) ;
#3758=CARTESIAN_POINT ( 'NONE',  ( -5.000000000000001776, 5.000000000000001776, 148.0000000000000284 ) ) ;
#3777=STYLED_ITEM ( 'NONE', ( #5219 ), #1900 ) ;
#3839=ORIENTED_EDGE ( 'NONE', *, *, #4580, .T. ) ;
#3846=VECTOR ( 'NONE', #3343, 1000.000000000000000 ) ;
#3851=VECTOR ( 'NONE', #2557, 1000.000000000000000 ) ;
#3855=DIRECTION ( 'NONE',  ( -1.734723475976806848E-16, -1.000000000000000000, 0.000000000000000000 ) ) ;
#3858=FACE_OUTER_BOUND ( 'NONE', #1580, .T. ) ;
#3881=CARTESIAN_POINT ( 'NONE',  ( 5.000000000000000000, -5.000000000000000000, 140.0000000000000000 ) ) ;
#3884=CARTESIAN_POINT ( 'NONE',  ( 0.000000000000000000, 0.000000000000000000, 148.0000000000000284 ) ) ;
#3889=FACE_OUTER_BOUND ( 'NONE', #6715, .T. ) ;
#3920=PRODUCT ( 'roller axis assy_r4', 'roller axis assy_r4', '', ( #3259 ) ) ;
#3933=UNCERTAINTY_MEASURE_WITH_UNIT (LENGTH_MEASURE( 1.000000000000000082E-05 ), #6030, 'distance_accuracy_value', 'NONE');
#3942=ADVANCED_FACE ( 'NONE', ( #3412, #624 ), #8599, .T. ) ;
#3965=DIRECTION ( 'NONE',  ( 1.000000000000000000, 0.000000000000000000, 0.000000000000000000 ) ) ;
#3970=FILL_AREA_STYLE_COLOUR ( '', #4051 ) ;
#3986=EDGE_CURVE ( 'NONE', #5212, #7983, #7328, .T. ) ;
#4022=DIRECTION ( 'NONE',  ( -0.000000000000000000, -0.000000000000000000, 1.000000000000000000 ) ) ;
#4030=CARTESIAN_POINT ( 'NONE',  ( 10.00000000000000000, 0.000000000000000000, 140.0000000000000000 ) ) ;
#4038=CARTESIAN_POINT ( 'NONE',  ( -10.00000000000000000, 1.224646799147353059E-15, 120.0000000000000284 ) ) ;
#4051=COLOUR_RGB ( '',0.8941176470588234615, 0.8941176470588234615, 0.8941176470588234615 ) ;
#4058=DIRECTION ( 'NONE',  ( 0.000000000000000000, 0.000000000000000000, -1.000000000000000000 ) ) ;
#4063=DIRECTION ( 'NONE',  ( -0.000000000000000000, -0.000000000000000000, 1.000000000000000000 ) ) ;
#4065=AXIS2_PLACEMENT_3D ( 'NONE', #6580, #4058, #8596 ) ;
#4073=CARTESIAN_POINT ( 'NONE',  ( -10.00000000000000000, 1.224646799147353059E-15, -7.999999999999996447 ) ) ;
#4075=FACE_OUTER_BOUND ( 'NONE', #7527, .T. ) ;
#4106=DIRECTION ( 'NONE',  ( -1.734723475976806848E-16, 1.000000000000000000, 0.000000000000000000 ) ) ;
#4119=ORIENTED_EDGE ( 'NONE', *, *, #4580, .F. ) ;
#4133=FACE_OUTER_BOUND ( 'NONE', #506, .T. ) ;
#4136=ORIENTED_EDGE ( 'NONE', *, *, #306, .F. ) ;
#4140=DIRECTION ( 'NONE',  ( -0.000000000000000000, -0.000000000000000000, 1.000000000000000000 ) ) ;
#4166=CARTESIAN_POINT ( 'NONE',  ( -5.000000000000000000, -5.000000000000000000, -27.99999999999999645 ) ) ;
#4179=LINE ( 'NONE', #6831, #7574 ) ;
#4195=EDGE_LOOP ( 'NONE', ( #862, #4405 ) ) ;
#4225=CARTESIAN_POINT ( 'NONE',  ( 10.00000000000000000, 0.000000000000000000, -27.99999999999999645 ) ) ;
#4253=ORIENTED_EDGE ( 'NONE', *, *, #5665, .T. ) ;
#4260=DIRECTION ( 'NONE',  ( -0.000000000000000000, -0.000000000000000000, 1.000000000000000000 ) ) ;
#4291=CARTESIAN_POINT ( 'NONE',  ( 5.000000000000000000, 5.000000000000000000, -27.99999999999999645 ) ) ;
#4316=EDGE_LOOP ( 'NONE', ( #7225, #521, #7494, #3289 ) ) ;
#4342=VECTOR ( 'NONE', #4022, 1000.000000000000000 ) ;
#4345=ORIENTED_EDGE ( 'NONE', *, *, #830, .T. ) ;
#4366=VECTOR ( 'NONE', #6498, 1000.000000000000000 ) ;
#4367=CARTESIAN_POINT ( 'NONE',  ( 20.00000000000000000, 0.000000000000000000, 120.0000000000000142 ) ) ;
#4391=EDGE_CURVE ( 'NONE', #563, #6628, #3340, .T. ) ;
#4402=VECTOR ( 'NONE', #6333, 1000.000000000000000 ) ;
#4405=ORIENTED_EDGE ( 'NONE', *, *, #1539, .F. ) ;
#4421=LINE ( 'NONE', #4291, #3704 ) ;
#4424=ORIENTED_EDGE ( 'NONE', *, *, #6500, .T. ) ;
#4431=ADVANCED_FACE ( 'NONE', ( #5000 ), #6345, .F. ) ;
#4448=LINE ( 'NONE', #490, #7695 ) ;
#4449=DIRECTION ( 'NONE',  ( 1.000000000000000000, -1.734723475976806848E-16, 0.000000000000000000 ) ) ;
#4450=AXIS2_PLACEMENT_3D ( 'NONE', #7754, #1087, #3698 ) ;
#4452=DIRECTION ( 'NONE',  ( 0.000000000000000000, 0.000000000000000000, 1.000000000000000000 ) ) ;
#4456=DIRECTION ( 'NONE',  ( -1.000000000000000000, 0.000000000000000000, -0.000000000000000000 ) ) ;
#4470=ORIENTED_EDGE ( 'NONE', *, *, #1539, .T. ) ;
#4481=VECTOR ( 'NONE', #7498, 1000.000000000000000 ) ;
#4515=VERTEX_POINT ( 'NONE', #8008 ) ;
#4537=DIRECTION ( 'NONE',  ( 1.000000000000000000, -1.734723475976806848E-16, 0.000000000000000000 ) ) ;
#4560=AXIS2_PLACEMENT_3D ( 'NONE', #5821, #2414, #391 ) ;
#4561=LINE ( 'NONE', #3881, #5123 ) ;
#4580=EDGE_CURVE ( 'NONE', #428, #7903, #5940, .T. ) ;
#4592=CARTESIAN_POINT ( 'NONE',  ( -5.000000000000000000, -5.000000000000000000, 140.0000000000000000 ) ) ;
#4601=CARTESIAN_POINT ( 'NONE',  ( 0.000000000000000000, 0.000000000000000000, -27.99999999999999645 ) ) ;
#4608=DIRECTION ( 'NONE',  ( 0.000000000000000000, 0.000000000000000000, -1.000000000000000000 ) ) ;
#4609=CARTESIAN_POINT ( 'NONE',  ( -10.00000000000000000, 1.224646799147353059E-15, 140.0000000000000000 ) ) ;
#4611=EDGE_CURVE ( 'NONE', #2181, #1089, #6815, .T. ) ;
#4616=ORIENTED_EDGE ( 'NONE', *, *, #2468, .T. ) ;
#4618=FACE_OUTER_BOUND ( 'NONE', #6283, .T. ) ;
#4628=CARTESIAN_POINT ( 'NONE',  ( -5.000000000000000000, -5.000000000000000000, 148.0000000000000284 ) ) ;
#4631=EDGE_LOOP ( 'NONE', ( #6769, #3267, #1001, #4691 ) ) ;
#4651=ORIENTED_EDGE ( 'NONE', *, *, #1589, .F. ) ;
#4683=DIRECTION ( 'NONE',  ( 0.000000000000000000, 0.000000000000000000, -1.000000000000000000 ) ) ;
#4686=MANIFOLD_SOLID_BREP ( 'Boss-Extrude4', #6195 ) ;
#4688=SHAPE_DEFINITION_REPRESENTATION ( #1345, #638 ) ;
#4691=ORIENTED_EDGE ( 'NONE', *, *, #2265, .T. ) ;
#4697=VERTEX_POINT ( 'NONE', #8429 ) ;
#4699=SURFACE_STYLE_FILL_AREA ( #8065 ) ;
#4713=PLANE ( 'NONE',  #7399 ) ;
#4737=FACE_OUTER_BOUND ( 'NONE', #5942, .T. ) ;
#4743=( NAMED_UNIT ( * ) SI_UNIT ( $, .STERADIAN. ) SOLID_ANGLE_UNIT ( ) );
#4766=ORIENTED_EDGE ( 'NONE', *, *, #1952, .T. ) ;
#4780=VERTEX_POINT ( 'NONE', #7230 ) ;
#4781=ADVANCED_FACE ( 'NONE', ( #800 ), #6050, .T. ) ;
#4804=ORIENTED_EDGE ( 'NONE', *, *, #1889, .T. ) ;
#4810=EDGE_CURVE ( 'NONE', #6932, #104, #1358, .T. ) ;
#4828=EDGE_CURVE ( 'NONE', #563, #6157, #1271, .T. ) ;
#4830=FACE_OUTER_BOUND ( 'NONE', #3724, .T. ) ;
#4839=ADVANCED_FACE ( 'NONE', ( #8035, #19 ), #2066, .F. ) ;
#4923=EDGE_CURVE ( 'NONE', #8570, #8480, #7450, .T. ) ;
#4949=VERTEX_POINT ( 'NONE', #8121 ) ;
#4976=CARTESIAN_POINT ( 'NONE',  ( 0.000000000000000000, 0.000000000000000000, 120.0000000000000142 ) ) ;
#4987=LINE ( 'NONE', #990, #7877 ) ;
#4995=DIRECTION ( 'NONE',  ( 0.000000000000000000, 0.000000000000000000, -1.000000000000000000 ) ) ;
#5000=FACE_OUTER_BOUND ( 'NONE', #2241, .T. ) ;
#5023=MECHANICAL_DESIGN_GEOMETRIC_PRESENTATION_REPRESENTATION('',(#7816),#721);
#5063=CARTESIAN_POINT ( 'NONE',  ( 5.000000000000000000, -5.000000000000000000, -36.00000000000000000 ) ) ;
#5076=ORIENTED_EDGE ( 'NONE', *, *, #8521, .T. ) ;
#5103=EDGE_CURVE ( 'NONE', #5212, #3427, #4448, .T. ) ;
#5116=ORIENTED_EDGE ( 'NONE', *, *, #4923, .F. ) ;
#5123=VECTOR ( 'NONE', #6650, 1000.000000000000000 ) ;
#5125=ORIENTED_EDGE ( 'NONE', *, *, #120, .F. ) ;
#5131=ORIENTED_EDGE ( 'NONE', *, *, #120, .T. ) ;
#5134=AXIS2_PLACEMENT_3D ( 'NONE', #6533, #4452, #7152 ) ;
#5142=AXIS2_PLACEMENT_3D ( 'NONE', #3328, #2026, #5968 ) ;
#5151=LINE ( 'NONE', #5964, #4366 ) ;
#5160=MECHANICAL_DESIGN_GEOMETRIC_PRESENTATION_REPRESENTATION('',(#3777),#2536);
#5184=AXIS2_PLACEMENT_3D ( 'NONE', #7378, #2807, #854 ) ;
#5197=LINE ( 'NONE', #4628, #3851 ) ;
#5200=CARTESIAN_POINT ( 'NONE',  ( -5.000000000000000000, -5.000000000000000000, -36.00000000000000000 ) ) ;
#5212=VERTEX_POINT ( 'NONE', #5910 ) ;
#5213=DIRECTION ( 'NONE',  ( -1.000000000000000000, 1.734723475976806848E-16, -0.000000000000000000 ) ) ;
#5217=ORIENTED_EDGE ( 'NONE', *, *, #1141, .F. ) ;
#5219=PRESENTATION_STYLE_ASSIGNMENT (( #613 ) ) ;
#5247=CARTESIAN_POINT ( 'NONE',  ( -5.000000000000000000, -5.000000000000000000, -36.00000000000000000 ) ) ;
#5253=ADVANCED_FACE ( 'NONE', ( #7886 ), #2095, .F. ) ;
#5267=DIRECTION ( 'NONE',  ( 1.000000000000000000, 0.000000000000000000, 0.000000000000000000 ) ) ;
#5294=LINE ( 'NONE', #1218, #2277 ) ;
#5308=CARTESIAN_POINT ( 'NONE',  ( 0.000000000000000000, 0.000000000000000000, -7.999999999999992895 ) ) ;
#5329=DIRECTION ( 'NONE',  ( 1.000000000000000000, 0.000000000000000000, 0.000000000000000000 ) ) ;
#5404=FACE_OUTER_BOUND ( 'NONE', #159, .T. ) ;
#5407=DIRECTION ( 'NONE',  ( 0.000000000000000000, 0.000000000000000000, -1.000000000000000000 ) ) ;
#5448=AXIS2_PLACEMENT_3D ( 'NONE', #4976, #7635, #1015 ) ;
#5455=VERTEX_POINT ( 'NONE', #8457 ) ;
#5460=ORIENTED_EDGE ( 'NONE', *, *, #8070, .F. ) ;
#5487=DIRECTION ( 'NONE',  ( -1.000000000000000000, 0.000000000000000000, 0.000000000000000000 ) ) ;
#5549=CARTESIAN_POINT ( 'NONE',  ( -5.000000000000000000, -5.000000000000000000, 148.0000000000000284 ) ) ;
#5554=ORIENTED_EDGE ( 'NONE', *, *, #5665, .F. ) ;
#5611=ORIENTED_EDGE ( 'NONE', *, *, #4391, .T. ) ;
#5637=CARTESIAN_POINT ( 'NONE',  ( 10.00000000000000000, 0.000000000000000000, 120.0000000000000284 ) ) ;
#5648=VECTOR ( 'NONE', #7330, 1000.000000000000000 ) ;
#5658=CARTESIAN_POINT ( 'NONE',  ( 0.000000000000000000, 0.000000000000000000, 120.0000000000000284 ) ) ;
#5665=EDGE_CURVE ( 'NONE', #7983, #7651, #5294, .T. ) ;
#5681=CARTESIAN_POINT ( 'NONE',  ( -5.000000000000001776, 5.000000000000001776, -36.00000000000000000 ) ) ;
#5702=ORIENTED_EDGE ( 'NONE', *, *, #299, .T. ) ;
#5764=DIRECTION ( 'NONE',  ( 1.000000000000000000, 0.000000000000000000, 0.000000000000000000 ) ) ;
#5771=EDGE_CURVE ( 'NONE', #7903, #2181, #2086, .T. ) ;
#5797=DIRECTION ( 'NONE',  ( -1.000000000000000000, 0.000000000000000000, -0.000000000000000000 ) ) ;
#5800=DIRECTION ( 'NONE',  ( 0.000000000000000000, 0.000000000000000000, -1.000000000000000000 ) ) ;
#5821=CARTESIAN_POINT ( 'NONE',  ( 0.000000000000000000, 0.000000000000000000, -84.56854249492380404 ) ) ;
#5823=EDGE_LOOP ( 'NONE', ( #8412, #4651 ) ) ;
#5896=DIRECTION ( 'NONE',  ( -1.000000000000000000, 0.000000000000000000, 0.000000000000000000 ) ) ;
#5910=CARTESIAN_POINT ( 'NONE',  ( 5.000000000000000000, 5.000000000000000000, 148.0000000000000284 ) ) ;
#5927=LINE ( 'NONE', #7287, #5648 ) ;
#5940=LINE ( 'NONE', #5247, #6281 ) ;
#5942=EDGE_LOOP ( 'NONE', ( #5116, #1457, #4424, #2078 ) ) ;
#5951=SURFACE_SIDE_STYLE ('',( #4699 ) ) ;
#5963=DIRECTION ( 'NONE',  ( -0.000000000000000000, -0.000000000000000000, 1.000000000000000000 ) ) ;
#5964=CARTESIAN_POINT ( 'NONE',  ( 10.00000000000000000, 0.000000000000000000, -27.99999999999999645 ) ) ;
#5968=DIRECTION ( 'NONE',  ( -1.000000000000000000, 0.000000000000000000, -0.000000000000000000 ) ) ;
#5988=CYLINDRICAL_SURFACE ( 'NONE', #7718, 10.00000000000000000 ) ;
#6030=( LENGTH_UNIT ( ) NAMED_UNIT ( * ) SI_UNIT ( .MILLI., .METRE. ) );
#6031=ORIENTED_EDGE ( 'NONE', *, *, #5771, .T. ) ;
#6036=DIRECTION ( 'NONE',  ( -1.000000000000000000, 0.000000000000000000, 0.000000000000000000 ) ) ;
#6050=CYLINDRICAL_SURFACE ( 'NONE', #23, 10.00000000000000000 ) ;
#6060=VERTEX_POINT ( 'NONE', #3251 ) ;
#6104=PLANE ( 'NONE',  #2429 ) ;
#6120=LINE ( 'NONE', #157, #7055 ) ;
#6129=PRODUCT_DEFINITION_FORMATION_WITH_SPECIFIED_SOURCE ( 'ANY', '', #3920, .NOT_KNOWN. ) ;
#6157=VERTEX_POINT ( 'NONE', #4073 ) ;
#6170=DIRECTION ( 'NONE',  ( 0.000000000000000000, 1.000000000000000000, 0.000000000000000000 ) ) ;
#6176=ORIENTED_EDGE ( 'NONE', *, *, #2468, .F. ) ;
#6185=LINE ( 'NONE', #7542, #4342 ) ;
#6195=CLOSED_SHELL ( 'NONE', ( #2924, #3562, #4781, #2216, #6530, #4431, #548, #2262, #2921, #2720, #3942, #8143, #2684, #5253, #7766, #7950, #7583, #1872, #4839, #6938 ) ) ;
#6196=CARTESIAN_POINT ( 'NONE',  ( 10.00000000000000000, 0.000000000000000000, -27.99999999999999645 ) ) ;
#6201=ORIENTED_EDGE ( 'NONE', *, *, #899, .F. ) ;
#6204=LINE ( 'NONE', #5549, #3384 ) ;
#6205=DIRECTION ( 'NONE',  ( 0.000000000000000000, -1.000000000000000000, 0.000000000000000000 ) ) ;
#6231=FACE_OUTER_BOUND ( 'NONE', #52, .T. ) ;
#6235=DIRECTION ( 'NONE',  ( -0.000000000000000000, -0.000000000000000000, 1.000000000000000000 ) ) ;
#6237=ORIENTED_EDGE ( 'NONE', *, *, #2741, .F. ) ;
#6246=CARTESIAN_POINT ( 'NONE',  ( -5.000000000000000000, -5.000000000000000000, -36.00000000000000000 ) ) ;
#6249=LINE ( 'NONE', #5681, #4402 ) ;
#6267=DIRECTION ( 'NONE',  ( -0.000000000000000000, -0.000000000000000000, 1.000000000000000000 ) ) ;
#6268=VERTEX_POINT ( 'NONE', #4030 ) ;
#6281=VECTOR ( 'NONE', #4063, 1000.000000000000000 ) ;
#6283=EDGE_LOOP ( 'NONE', ( #1139, #5217, #8366, #3164 ) ) ;
#6308=ORIENTED_EDGE ( 'NONE', *, *, #2791, .F. ) ;
#6313=DIRECTION ( 'NONE',  ( -1.000000000000000000, 0.000000000000000000, -0.000000000000000000 ) ) ;
#6333=DIRECTION ( 'NONE',  ( 1.000000000000000000, -1.734723475976806848E-16, 0.000000000000000000 ) ) ;
#6345=PLANE ( 'NONE',  #7369 ) ;
#6347=ORIENTED_EDGE ( 'NONE', *, *, #11, .F. ) ;
#6355=FACE_OUTER_BOUND ( 'NONE', #4316, .T. ) ;
#6359=ORIENTED_EDGE ( 'NONE', *, *, #1740, .T. ) ;
#6362=CARTESIAN_POINT ( 'NONE',  ( -10.00000000000000000, 1.224646799147353059E-15, -27.99999999999999645 ) ) ;
#6372=UNCERTAINTY_MEASURE_WITH_UNIT (LENGTH_MEASURE( 1.000000000000000082E-05 ), #657, 'distance_accuracy_value', 'NONE');
#6447=EDGE_LOOP ( 'NONE', ( #6176, #838 ) ) ;
#6493=PLANE ( 'NONE',  #2333 ) ;
#6498=DIRECTION ( 'NONE',  ( -0.000000000000000000, -0.000000000000000000, 1.000000000000000000 ) ) ;
#6500=EDGE_CURVE ( 'NONE', #342, #6268, #5151, .T. ) ;
#6502=DIRECTION ( 'NONE',  ( 0.000000000000000000, 0.000000000000000000, 1.000000000000000000 ) ) ;
#6526=ORIENTED_EDGE ( 'NONE', *, *, #4611, .F. ) ;
#6530=ADVANCED_FACE ( 'NONE', ( #498, #1856 ), #7107, .T. ) ;
#6533=CARTESIAN_POINT ( 'NONE',  ( 0.000000000000000000, 0.000000000000000000, -84.56854249492380404 ) ) ;
#6567=SHAPE_REPRESENTATION_RELATIONSHIP ( 'NONE' , 'NONE' ,  #638, #1900 ) ;
#6571=VECTOR ( 'NONE', #5329, 1000.000000000000000 ) ;
#6576=APPLICATION_CONTEXT ( 'automotive_design' ) ;
#6580=CARTESIAN_POINT ( 'NONE',  ( 0.000000000000000000, 0.000000000000000000, 140.0000000000000000 ) ) ;
#6583=VECTOR ( 'NONE', #3221, 1000.000000000000000 ) ;
#6628=VERTEX_POINT ( 'NONE', #4225 ) ;
#6647=LINE ( 'NONE', #6687, #6583 ) ;
#6650=DIRECTION ( 'NONE',  ( 0.000000000000000000, 1.000000000000000000, 0.000000000000000000 ) ) ;
#6682=ORIENTED_EDGE ( 'NONE', *, *, #7044, .T. ) ;
#6684=EDGE_CURVE ( 'NONE', #3427, #7651, #4179, .T. ) ;
#6687=CARTESIAN_POINT ( 'NONE',  ( 5.000000000000000000, -5.000000000000000000, -27.99999999999999645 ) ) ;
#6688=CARTESIAN_POINT ( 'NONE',  ( 0.000000000000000000, 0.000000000000000000, -27.99999999999999645 ) ) ;
#6715=EDGE_LOOP ( 'NONE', ( #4616, #5702, #3432, #6201 ) ) ;
#6717=ORIENTED_EDGE ( 'NONE', *, *, #5771, .F. ) ;
#6720=DIRECTION ( 'NONE',  ( 0.000000000000000000, 1.000000000000000000, 0.000000000000000000 ) ) ;
#6736=EDGE_CURVE ( 'NONE', #35, #428, #1003, .T. ) ;
#6768=DIRECTION ( 'NONE',  ( -1.734723475976806848E-16, 1.000000000000000000, 0.000000000000000000 ) ) ;
#6769=ORIENTED_EDGE ( 'NONE', *, *, #4611, .T. ) ;
#6793=AXIS2_PLACEMENT_3D ( 'NONE', #8147, #4260, #7394 ) ;
#6811=ORIENTED_EDGE ( 'NONE', *, *, #1626, .T. ) ;
#6815=LINE ( 'NONE', #1384, #7111 ) ;
#6818=DIRECTION ( 'NONE',  ( -1.734723475976806848E-16, 1.000000000000000000, 0.000000000000000000 ) ) ;
#6831=CARTESIAN_POINT ( 'NONE',  ( -5.000000000000001776, 5.000000000000001776, 148.0000000000000284 ) ) ;
#6861=APPLICATION_CONTEXT ( 'automotive_design' ) ;
#6887=PLANE ( 'NONE',  #5448 ) ;
#6932=VERTEX_POINT ( 'NONE', #560 ) ;
#6938=ADVANCED_FACE ( 'NONE', ( #4737 ), #5988, .T. ) ;
#6963=FACE_OUTER_BOUND ( 'NONE', #6973, .T. ) ;
#6967=ORIENTED_EDGE ( 'NONE', *, *, #6500, .F. ) ;
#6973=EDGE_LOOP ( 'NONE', ( #6811, #2618, #619, #2730 ) ) ;
#7044=EDGE_CURVE ( 'NONE', #3680, #7903, #6647, .T. ) ;
#7055=VECTOR ( 'NONE', #8149, 1000.000000000000000 ) ;
#7071=UNCERTAINTY_MEASURE_WITH_UNIT (LENGTH_MEASURE( 1.000000000000000082E-05 ), #743, 'distance_accuracy_value', 'NONE');
#7107=PLANE ( 'NONE',  #8273 ) ;
#7111=VECTOR ( 'NONE', #3431, 1000.000000000000000 ) ;
#7143=ORIENTED_EDGE ( 'NONE', *, *, #2741, .T. ) ;
#7152=DIRECTION ( 'NONE',  ( 1.000000000000000000, 0.000000000000000000, 0.000000000000000000 ) ) ;
#7168=DIRECTION ( 'NONE',  ( 0.000000000000000000, 0.000000000000000000, 1.000000000000000000 ) ) ;
#7173=AXIS2_PLACEMENT_3D ( 'NONE', #772, #278, #8136 ) ;
#7203=LINE ( 'NONE', #4592, #6571 ) ;
#7225=ORIENTED_EDGE ( 'NONE', *, *, #299, .F. ) ;
#7228=DIRECTION ( 'NONE',  ( 0.000000000000000000, 0.000000000000000000, 1.000000000000000000 ) ) ;
#7229=PRODUCT_DEFINITION ( 'UNKNOWN', '', #6129, #7244 ) ;
#7230=CARTESIAN_POINT ( 'NONE',  ( -20.00000000000000000, 2.449293598294706513E-15, 120.0000000000000142 ) ) ;
#7235=DIRECTION ( 'NONE',  ( -1.000000000000000000, 0.000000000000000000, 0.000000000000000000 ) ) ;
#7244=PRODUCT_DEFINITION_CONTEXT ( 'detailed design', #6861, 'design' ) ;
#7253=EDGE_LOOP ( 'NONE', ( #5131, #2308, #4804, #5076 ) ) ;
#7275=VERTEX_POINT ( 'NONE', #994 ) ;
#7279=CARTESIAN_POINT ( 'NONE',  ( 0.000000000000000000, 0.000000000000000000, -27.99999999999999645 ) ) ;
#7287=CARTESIAN_POINT ( 'NONE',  ( -5.000000000000000000, -5.000000000000000000, 148.0000000000000284 ) ) ;
#7298=LINE ( 'NONE', #775, #3846 ) ;
#7328=LINE ( 'NONE', #8080, #1816 ) ;
#7330=DIRECTION ( 'NONE',  ( 1.734723475976806848E-16, -1.000000000000000000, -0.000000000000000000 ) ) ;
#7332=ORIENTED_EDGE ( 'NONE', *, *, #8521, .F. ) ;
#7336=AXIS2_PLACEMENT_3D ( 'NONE', #3154, #5797, #7811 ) ;
#7366=CARTESIAN_POINT ( 'NONE',  ( 5.000000000000000000, -5.000000000000000000, 148.0000000000000284 ) ) ;
#7369=AXIS2_PLACEMENT_3D ( 'NONE', #8454, #294, #1830 ) ;
#7373=ORIENTED_EDGE ( 'NONE', *, *, #8388, .T. ) ;
#7378=CARTESIAN_POINT ( 'NONE',  ( 0.000000000000000000, 0.000000000000000000, 120.0000000000000142 ) ) ;
#7394=DIRECTION ( 'NONE',  ( 1.000000000000000000, 0.000000000000000000, 0.000000000000000000 ) ) ;
#7399=AXIS2_PLACEMENT_3D ( 'NONE', #2798, #1496, #4106 ) ;
#7402=CIRCLE ( 'NONE', #1719, 20.00000000000000000 ) ;
#7409=DIRECTION ( 'NONE',  ( 1.000000000000000000, 0.000000000000000000, 0.000000000000000000 ) ) ;
#7427=ORIENTED_EDGE ( 'NONE', *, *, #4391, .F. ) ;
#7450=LINE ( 'NONE', #3621, #4481 ) ;
#7451=EDGE_CURVE ( 'NONE', #7275, #104, #7203, .T. ) ;
#7494=ORIENTED_EDGE ( 'NONE', *, *, #899, .T. ) ;
#7498=DIRECTION ( 'NONE',  ( -0.000000000000000000, -0.000000000000000000, 1.000000000000000000 ) ) ;
#7504=CARTESIAN_POINT ( 'NONE',  ( 0.000000000000000000, 0.000000000000000000, -7.999999999999992895 ) ) ;
#7518=ORIENTED_EDGE ( 'NONE', *, *, #8070, .T. ) ;
#7527=EDGE_LOOP ( 'NONE', ( #7883, #7666, #7332, #4766 ) ) ;
#7542=CARTESIAN_POINT ( 'NONE',  ( 5.000000000000000000, -5.000000000000000000, -36.00000000000000000 ) ) ;
#7557=EDGE_CURVE ( 'NONE', #8142, #4780, #317, .T. ) ;
#7574=VECTOR ( 'NONE', #2918, 1000.000000000000000 ) ;
#7583=ADVANCED_FACE ( 'NONE', ( #4075 ), #6104, .F. ) ;
#7635=DIRECTION ( 'NONE',  ( 0.000000000000000000, 0.000000000000000000, 1.000000000000000000 ) ) ;
#7651=VERTEX_POINT ( 'NONE', #2300 ) ;
#7666=ORIENTED_EDGE ( 'NONE', *, *, #4810, .F. ) ;
#7681=ORIENTED_EDGE ( 'NONE', *, *, #7044, .F. ) ;
#7695=VECTOR ( 'NONE', #531, 1000.000000000000000 ) ;
#7702=EDGE_LOOP ( 'NONE', ( #6717, #7681, #61, #6526 ) ) ;
#7718=AXIS2_PLACEMENT_3D ( 'NONE', #4601, #8536, #3965 ) ;
#7730=LINE ( 'NONE', #8383, #935 ) ;
#7743=EDGE_LOOP ( 'NONE', ( #1047, #5611 ) ) ;
#7752=AXIS2_PLACEMENT_3D ( 'NONE', #572, #1268, #3197 ) ;
#7754=CARTESIAN_POINT ( 'NONE',  ( 0.000000000000000000, 0.000000000000000000, -27.99999999999999645 ) ) ;
#7761=CYLINDRICAL_SURFACE ( 'NONE', #4560, 20.00000000000000000 ) ;
#7766=ADVANCED_FACE ( 'NONE', ( #2673 ), #1274, .F. ) ;
#7772=AXIS2_PLACEMENT_3D ( 'NONE', #5658, #695, #1221 ) ;
#7811=DIRECTION ( 'NONE',  ( -0.000000000000000000, 0.000000000000000000, 1.000000000000000000 ) ) ;
#7815=CIRCLE ( 'NONE', #7772, 10.00000000000000000 ) ;
#7816=STYLED_ITEM('',(#8678),#4686);
#7841=AXIS2_PLACEMENT_3D ( 'NONE', #7896, #3855, #4537 ) ;
#7877=VECTOR ( 'NONE', #281, 1000.000000000000000 ) ;
#7883=ORIENTED_EDGE ( 'NONE', *, *, #7451, .T. ) ;
#7886=FACE_OUTER_BOUND ( 'NONE', #7253, .T. ) ;
#7896=CARTESIAN_POINT ( 'NONE',  ( -5.000000000000001776, 5.000000000000001776, 148.0000000000000284 ) ) ;
#7903=VERTEX_POINT ( 'NONE', #3327 ) ;
#7909=CIRCLE ( 'NONE', #390, 20.00000000000000000 ) ;
#7912=DIRECTION ( 'NONE',  ( 1.000000000000000000, 0.000000000000000000, 0.000000000000000000 ) ) ;
#7925=ORIENTED_EDGE ( 'NONE', *, *, #1589, .T. ) ;
#7950=ADVANCED_FACE ( 'NONE', ( #5404 ), #4713, .F. ) ;
#7983=VERTEX_POINT ( 'NONE', #221 ) ;
#8008=CARTESIAN_POINT ( 'NONE',  ( -5.000000000000000000, -5.000000000000000000, 148.0000000000000284 ) ) ;
#8017=CARTESIAN_POINT ( 'NONE',  ( 5.000000000000000000, 5.000000000000000000, -27.99999999999999645 ) ) ;
#8035=FACE_OUTER_BOUND ( 'NONE', #5823, .T. ) ;
#8065=FILL_AREA_STYLE ('',( #3970 ) ) ;
#8070=EDGE_CURVE ( 'NONE', #35, #3680, #6185, .T. ) ;
#8080=CARTESIAN_POINT ( 'NONE',  ( 5.000000000000000000, 5.000000000000000000, 148.0000000000000284 ) ) ;
#8081=DIRECTION ( 'NONE',  ( -1.000000000000000000, 0.000000000000000000, 0.000000000000000000 ) ) ;
#8120=AXIS2_PLACEMENT_3D ( 'NONE', #3884, #4608, #1260 ) ;
#8121=CARTESIAN_POINT ( 'NONE',  ( -5.000000000000001776, 5.000000000000001776, -36.00000000000000000 ) ) ;
#8136=DIRECTION ( 'NONE',  ( -1.000000000000000000, 0.000000000000000000, 0.000000000000000000 ) ) ;
#8142=VERTEX_POINT ( 'NONE', #4367 ) ;
#8143=ADVANCED_FACE ( 'NONE', ( #1629, #6231 ), #6887, .T. ) ;
#8147=CARTESIAN_POINT ( 'NONE',  ( 0.000000000000000000, 0.000000000000000000, -27.99999999999999645 ) ) ;
#8149=DIRECTION ( 'NONE',  ( -0.000000000000000000, -0.000000000000000000, 1.000000000000000000 ) ) ;
#8198=CARTESIAN_POINT ( 'NONE',  ( 20.00000000000000000, 0.000000000000000000, -84.56854249492380404 ) ) ;
#8273=AXIS2_PLACEMENT_3D ( 'NONE', #7279, #5800, #4456 ) ;
#8296=CIRCLE ( 'NONE', #209, 10.00000000000000000 ) ;
#8351=CARTESIAN_POINT ( 'NONE',  ( 5.000000000000000000, 5.000000000000000000, -36.00000000000000000 ) ) ;
#8366=ORIENTED_EDGE ( 'NONE', *, *, #11, .T. ) ;
#8383=CARTESIAN_POINT ( 'NONE',  ( -5.000000000000000000, -5.000000000000000000, 140.0000000000000000 ) ) ;
#8385=VECTOR ( 'NONE', #2717, 1000.000000000000000 ) ;
#8388=EDGE_CURVE ( 'NONE', #4780, #8142, #7402, .T. ) ;
#8395=ORIENTED_EDGE ( 'NONE', *, *, #7451, .F. ) ;
#8412=ORIENTED_EDGE ( 'NONE', *, *, #3296, .F. ) ;
#8429=CARTESIAN_POINT ( 'NONE',  ( 10.00000000000000000, 0.000000000000000000, -7.999999999999996447 ) ) ;
#8451=AXIS2_PLACEMENT_3D ( 'NONE', #114, #7228, #5267 ) ;
#8454=CARTESIAN_POINT ( 'NONE',  ( -5.000000000000000000, -5.000000000000000000, -36.00000000000000000 ) ) ;
#8457=CARTESIAN_POINT ( 'NONE',  ( 5.000000000000000000, 5.000000000000000000, -36.00000000000000000 ) ) ;
#8480=VERTEX_POINT ( 'NONE', #4609 ) ;
#8496=CARTESIAN_POINT ( 'NONE',  ( 0.000000000000000000, 0.000000000000000000, -36.00000000000000000 ) ) ;
#8505=PLANE ( 'NONE',  #7336 ) ;
#8521=EDGE_CURVE ( 'NONE', #4515, #6932, #6204, .T. ) ;
#8523=VECTOR ( 'NONE', #6818, 1000.000000000000000 ) ;
#8536=DIRECTION ( 'NONE',  ( -0.000000000000000000, -0.000000000000000000, 1.000000000000000000 ) ) ;
#8545=ORIENTED_EDGE ( 'NONE', *, *, #4923, .T. ) ;
#8570=VERTEX_POINT ( 'NONE', #4038 ) ;
#8596=DIRECTION ( 'NONE',  ( -1.000000000000000000, 0.000000000000000000, -0.000000000000000000 ) ) ;
#8599=PLANE ( 'NONE',  #5142 ) ;
#8600=DIRECTION ( 'NONE',  ( -1.000000000000000000, 0.000000000000000000, 0.000000000000000000 ) ) ;
#8672=COLOUR_RGB('Off White',0.89,0.88,0.83);
#8673=FILL_AREA_STYLE_COLOUR('',#8672);
#8674=FILL_AREA_STYLE('',(#8673));
#8675=SURFACE_STYLE_FILL_AREA(#8674);
#8676=SURFACE_SIDE_STYLE('',(#8675));
#8677=SURFACE_STYLE_USAGE(.BOTH.,#8676);
#8678=PRESENTATION_STYLE_ASSIGNMENT((#8677));
ENDSEC;
END-ISO-10303-21;
